ISO-10303-21;
HEADER;
/* Generated by software containing ST-Developer
 * from STEP Tools, Inc. (www.steptools.com) 
 */

FILE_DESCRIPTION(
/* description */ ('PAT-003'),
/* implementation_level */ '2;1');

FILE_NAME(
/* name */ 'Cap Screw - M4x16.step',
/* time_stamp */ '2026-10-29T15:45:40-07:00',
/* author */ (''),
/* organization */ (''),
/* preprocessor_version */ 'ST-DEVELOPER v20.2',
/* originating_system */ 'Autodesk Translation Framework v15.17.0.0',
/* authorisation */ '');

FILE_SCHEMA (('AUTOMOTIVE_DESIGN { 1 0 10303 214 3 1 1 }'));
ENDSEC;

DATA;
#10=MECHANICAL_DESIGN_GEOMETRIC_PRESENTATION_REPRESENTATION('',(#155),#5761);
#106=ORIENTED_CLOSED_SHELL('',*,#3331,.F.);
#108=BREP_WITH_VOIDS('Body1',#3330,(#106));
#115=CONICAL_SURFACE('',#3671,0.325,0.785398163397448);
#116=CONICAL_SURFACE('',#3675,0.335,0.785398163397448);
#117=CONICAL_SURFACE('',#3679,0.21,0.463647609000806);
#118=CONICAL_SURFACE('',#3683,0.18,0.785398163397448);
#131=SHAPE_REPRESENTATION_RELATIONSHIP('SRR','None',#5826,#143);
#143=ADVANCED_BREP_SHAPE_REPRESENTATION('',(#108),#5757);
#155=STYLED_ITEM('',(#5956),#108);
#198=FACE_BOUND('',#695,.T.);
#311=PLANE('',#3669);
#312=PLANE('',#3677);
#313=PLANE('',#3685);
#314=PLANE('',#3686);
#315=PLANE('',#3687);
#316=PLANE('',#3688);
#317=PLANE('',#3689);
#318=PLANE('',#3690);
#319=PLANE('',#3691);
#320=PLANE('',#3692);
#321=PLANE('',#3693);
#474=FACE_OUTER_BOUND('',#690,.T.);
#475=FACE_OUTER_BOUND('',#691,.T.);
#476=FACE_OUTER_BOUND('',#692,.T.);
#477=FACE_OUTER_BOUND('',#693,.T.);
#478=FACE_OUTER_BOUND('',#694,.T.);
#479=FACE_OUTER_BOUND('',#696,.T.);
#480=FACE_OUTER_BOUND('',#697,.T.);
#481=FACE_OUTER_BOUND('',#698,.T.);
#482=FACE_OUTER_BOUND('',#699,.T.);
#483=FACE_OUTER_BOUND('',#700,.T.);
#484=FACE_OUTER_BOUND('',#701,.T.);
#485=FACE_OUTER_BOUND('',#702,.T.);
#486=FACE_OUTER_BOUND('',#703,.T.);
#487=FACE_OUTER_BOUND('',#704,.T.);
#488=FACE_OUTER_BOUND('',#705,.T.);
#489=FACE_OUTER_BOUND('',#706,.T.);
#490=FACE_OUTER_BOUND('',#707,.T.);
#690=EDGE_LOOP('',(#2854));
#691=EDGE_LOOP('',(#2855,#2856,#2857,#2858));
#692=EDGE_LOOP('',(#2859,#2860,#2861,#2862));
#693=EDGE_LOOP('',(#2863,#2864,#2865,#2866));
#694=EDGE_LOOP('',(#2867));
#695=EDGE_LOOP('',(#2868));
#696=EDGE_LOOP('',(#2869,#2870,#2871,#2872));
#697=EDGE_LOOP('',(#2873,#2874,#2875,#2876));
#698=EDGE_LOOP('',(#2877,#2878,#2879,#2880));
#699=EDGE_LOOP('',(#2881));
#700=EDGE_LOOP('',(#2882,#2883,#2884,#2885));
#701=EDGE_LOOP('',(#2886,#2887,#2888,#2889));
#702=EDGE_LOOP('',(#2890,#2891,#2892,#2893));
#703=EDGE_LOOP('',(#2894,#2895,#2896,#2897));
#704=EDGE_LOOP('',(#2898,#2899,#2900,#2901));
#705=EDGE_LOOP('',(#2902,#2903,#2904,#2905));
#706=EDGE_LOOP('',(#2906,#2907,#2908,#2909,#2910,#2911));
#707=EDGE_LOOP('',(#2912,#2913,#2914,#2915,#2916,#2917));
#1008=LINE('',#5438,#1330);
#1009=LINE('',#5442,#1331);
#1010=LINE('',#5446,#1332);
#1011=LINE('',#5453,#1333);
#1012=LINE('',#5457,#1334);
#1013=LINE('',#5461,#1335);
#1014=LINE('',#5466,#1336);
#1015=LINE('',#5468,#1337);
#1016=LINE('',#5470,#1338);
#1017=LINE('',#5471,#1339);
#1018=LINE('',#5474,#1340);
#1019=LINE('',#5476,#1341);
#1020=LINE('',#5477,#1342);
#1021=LINE('',#5480,#1343);
#1022=LINE('',#5482,#1344);
#1023=LINE('',#5483,#1345);
#1024=LINE('',#5486,#1346);
#1025=LINE('',#5488,#1347);
#1026=LINE('',#5489,#1348);
#1027=LINE('',#5492,#1349);
#1028=LINE('',#5494,#1350);
#1029=LINE('',#5495,#1351);
#1030=LINE('',#5497,#1352);
#1031=LINE('',#5498,#1353);
#1330=VECTOR('',#4453,0.325);
#1331=VECTOR('',#4458,0.35);
#1332=VECTOR('',#4463,0.335);
#1333=VECTOR('',#4472,0.21);
#1334=VECTOR('',#4477,0.2);
#1335=VECTOR('',#4482,0.18);
#1336=VECTOR('',#4487,1.);
#1337=VECTOR('',#4488,1.);
#1338=VECTOR('',#4489,1.);
#1339=VECTOR('',#4490,1.);
#1340=VECTOR('',#4493,1.);
#1341=VECTOR('',#4494,1.);
#1342=VECTOR('',#4495,1.);
#1343=VECTOR('',#4498,1.);
#1344=VECTOR('',#4499,1.);
#1345=VECTOR('',#4500,1.);
#1346=VECTOR('',#4503,1.);
#1347=VECTOR('',#4504,1.);
#1348=VECTOR('',#4505,1.);
#1349=VECTOR('',#4508,1.);
#1350=VECTOR('',#4509,1.);
#1351=VECTOR('',#4510,1.);
#1352=VECTOR('',#4513,1.);
#1353=VECTOR('',#4514,1.);
#1450=CIRCLE('',#3670,0.3);
#1451=CIRCLE('',#3672,0.35);
#1452=CIRCLE('',#3674,0.35);
#1453=CIRCLE('',#3676,0.32);
#1454=CIRCLE('',#3678,0.22);
#1455=CIRCLE('',#3680,0.1954);
#1456=CIRCLE('',#3682,0.1954);
#1457=CIRCLE('',#3684,0.16);
#1702=VERTEX_POINT('',#5433);
#1703=VERTEX_POINT('',#5436);
#1704=VERTEX_POINT('',#5440);
#1705=VERTEX_POINT('',#5444);
#1706=VERTEX_POINT('',#5448);
#1707=VERTEX_POINT('',#5451);
#1708=VERTEX_POINT('',#5455);
#1709=VERTEX_POINT('',#5459);
#1710=VERTEX_POINT('',#5464);
#1711=VERTEX_POINT('',#5465);
#1712=VERTEX_POINT('',#5467);
#1713=VERTEX_POINT('',#5469);
#1714=VERTEX_POINT('',#5473);
#1715=VERTEX_POINT('',#5475);
#1716=VERTEX_POINT('',#5479);
#1717=VERTEX_POINT('',#5481);
#1718=VERTEX_POINT('',#5485);
#1719=VERTEX_POINT('',#5487);
#1720=VERTEX_POINT('',#5491);
#1721=VERTEX_POINT('',#5493);
#2098=EDGE_CURVE('',#1702,#1702,#1450,.T.);
#2099=EDGE_CURVE('',#1703,#1703,#1451,.T.);
#2100=EDGE_CURVE('',#1703,#1702,#1008,.T.);
#2101=EDGE_CURVE('',#1704,#1704,#1452,.T.);
#2102=EDGE_CURVE('',#1704,#1703,#1009,.T.);
#2103=EDGE_CURVE('',#1705,#1705,#1453,.T.);
#2104=EDGE_CURVE('',#1705,#1704,#1010,.T.);
#2105=EDGE_CURVE('',#1706,#1706,#1454,.T.);
#2106=EDGE_CURVE('',#1707,#1707,#1455,.F.);
#2107=EDGE_CURVE('',#1707,#1706,#1011,.T.);
#2108=EDGE_CURVE('',#1708,#1708,#1456,.F.);
#2109=EDGE_CURVE('',#1708,#1707,#1012,.T.);
#2110=EDGE_CURVE('',#1709,#1709,#1457,.T.);
#2111=EDGE_CURVE('',#1709,#1708,#1013,.T.);
#2112=EDGE_CURVE('',#1710,#1711,#1014,.T.);
#2113=EDGE_CURVE('',#1711,#1712,#1015,.T.);
#2114=EDGE_CURVE('',#1712,#1713,#1016,.T.);
#2115=EDGE_CURVE('',#1710,#1713,#1017,.T.);
#2116=EDGE_CURVE('',#1711,#1714,#1018,.T.);
#2117=EDGE_CURVE('',#1714,#1715,#1019,.T.);
#2118=EDGE_CURVE('',#1715,#1712,#1020,.T.);
#2119=EDGE_CURVE('',#1714,#1716,#1021,.T.);
#2120=EDGE_CURVE('',#1716,#1717,#1022,.T.);
#2121=EDGE_CURVE('',#1717,#1715,#1023,.T.);
#2122=EDGE_CURVE('',#1716,#1718,#1024,.T.);
#2123=EDGE_CURVE('',#1718,#1719,#1025,.T.);
#2124=EDGE_CURVE('',#1719,#1717,#1026,.T.);
#2125=EDGE_CURVE('',#1718,#1720,#1027,.T.);
#2126=EDGE_CURVE('',#1720,#1721,#1028,.T.);
#2127=EDGE_CURVE('',#1721,#1719,#1029,.T.);
#2128=EDGE_CURVE('',#1720,#1710,#1030,.T.);
#2129=EDGE_CURVE('',#1713,#1721,#1031,.T.);
#2854=ORIENTED_EDGE('',*,*,#2098,.F.);
#2855=ORIENTED_EDGE('',*,*,#2099,.F.);
#2856=ORIENTED_EDGE('',*,*,#2100,.T.);
#2857=ORIENTED_EDGE('',*,*,#2098,.T.);
#2858=ORIENTED_EDGE('',*,*,#2100,.F.);
#2859=ORIENTED_EDGE('',*,*,#2101,.F.);
#2860=ORIENTED_EDGE('',*,*,#2102,.T.);
#2861=ORIENTED_EDGE('',*,*,#2099,.T.);
#2862=ORIENTED_EDGE('',*,*,#2102,.F.);
#2863=ORIENTED_EDGE('',*,*,#2103,.F.);
#2864=ORIENTED_EDGE('',*,*,#2104,.T.);
#2865=ORIENTED_EDGE('',*,*,#2101,.T.);
#2866=ORIENTED_EDGE('',*,*,#2104,.F.);
#2867=ORIENTED_EDGE('',*,*,#2103,.T.);
#2868=ORIENTED_EDGE('',*,*,#2105,.F.);
#2869=ORIENTED_EDGE('',*,*,#2106,.F.);
#2870=ORIENTED_EDGE('',*,*,#2107,.T.);
#2871=ORIENTED_EDGE('',*,*,#2105,.T.);
#2872=ORIENTED_EDGE('',*,*,#2107,.F.);
#2873=ORIENTED_EDGE('',*,*,#2108,.F.);
#2874=ORIENTED_EDGE('',*,*,#2109,.T.);
#2875=ORIENTED_EDGE('',*,*,#2106,.T.);
#2876=ORIENTED_EDGE('',*,*,#2109,.F.);
#2877=ORIENTED_EDGE('',*,*,#2110,.F.);
#2878=ORIENTED_EDGE('',*,*,#2111,.T.);
#2879=ORIENTED_EDGE('',*,*,#2108,.T.);
#2880=ORIENTED_EDGE('',*,*,#2111,.F.);
#2881=ORIENTED_EDGE('',*,*,#2110,.T.);
#2882=ORIENTED_EDGE('',*,*,#2112,.T.);
#2883=ORIENTED_EDGE('',*,*,#2113,.T.);
#2884=ORIENTED_EDGE('',*,*,#2114,.T.);
#2885=ORIENTED_EDGE('',*,*,#2115,.F.);
#2886=ORIENTED_EDGE('',*,*,#2116,.T.);
#2887=ORIENTED_EDGE('',*,*,#2117,.T.);
#2888=ORIENTED_EDGE('',*,*,#2118,.T.);
#2889=ORIENTED_EDGE('',*,*,#2113,.F.);
#2890=ORIENTED_EDGE('',*,*,#2119,.T.);
#2891=ORIENTED_EDGE('',*,*,#2120,.T.);
#2892=ORIENTED_EDGE('',*,*,#2121,.T.);
#2893=ORIENTED_EDGE('',*,*,#2117,.F.);
#2894=ORIENTED_EDGE('',*,*,#2122,.T.);
#2895=ORIENTED_EDGE('',*,*,#2123,.T.);
#2896=ORIENTED_EDGE('',*,*,#2124,.T.);
#2897=ORIENTED_EDGE('',*,*,#2120,.F.);
#2898=ORIENTED_EDGE('',*,*,#2125,.T.);
#2899=ORIENTED_EDGE('',*,*,#2126,.T.);
#2900=ORIENTED_EDGE('',*,*,#2127,.T.);
#2901=ORIENTED_EDGE('',*,*,#2123,.F.);
#2902=ORIENTED_EDGE('',*,*,#2128,.T.);
#2903=ORIENTED_EDGE('',*,*,#2115,.T.);
#2904=ORIENTED_EDGE('',*,*,#2129,.T.);
#2905=ORIENTED_EDGE('',*,*,#2126,.F.);
#2906=ORIENTED_EDGE('',*,*,#2128,.F.);
#2907=ORIENTED_EDGE('',*,*,#2125,.F.);
#2908=ORIENTED_EDGE('',*,*,#2122,.F.);
#2909=ORIENTED_EDGE('',*,*,#2119,.F.);
#2910=ORIENTED_EDGE('',*,*,#2116,.F.);
#2911=ORIENTED_EDGE('',*,*,#2112,.F.);
#2912=ORIENTED_EDGE('',*,*,#2129,.F.);
#2913=ORIENTED_EDGE('',*,*,#2114,.F.);
#2914=ORIENTED_EDGE('',*,*,#2118,.F.);
#2915=ORIENTED_EDGE('',*,*,#2121,.F.);
#2916=ORIENTED_EDGE('',*,*,#2124,.F.);
#2917=ORIENTED_EDGE('',*,*,#2127,.F.);
#3116=CYLINDRICAL_SURFACE('',#3673,0.35);
#3117=CYLINDRICAL_SURFACE('',#3681,0.1954);
#3267=ADVANCED_FACE('',(#474),#311,.T.);
#3268=ADVANCED_FACE('',(#475),#115,.T.);
#3269=ADVANCED_FACE('',(#476),#3116,.T.);
#3270=ADVANCED_FACE('',(#477),#116,.T.);
#3271=ADVANCED_FACE('',(#478,#198),#312,.T.);
#3272=ADVANCED_FACE('',(#479),#117,.T.);
#3273=ADVANCED_FACE('',(#480),#3117,.T.);
#3274=ADVANCED_FACE('',(#481),#118,.T.);
#3275=ADVANCED_FACE('',(#482),#313,.T.);
#3276=ADVANCED_FACE('',(#483),#314,.F.);
#3277=ADVANCED_FACE('',(#484),#315,.F.);
#3278=ADVANCED_FACE('',(#485),#316,.F.);
#3279=ADVANCED_FACE('',(#486),#317,.F.);
#3280=ADVANCED_FACE('',(#487),#318,.F.);
#3281=ADVANCED_FACE('',(#488),#319,.F.);
#3282=ADVANCED_FACE('',(#489),#320,.F.);
#3283=ADVANCED_FACE('',(#490),#321,.F.);
#3330=CLOSED_SHELL('',(#3267,#3268,#3269,#3270,#3271,#3272,#3273,#3274,
#3275));
#3331=CLOSED_SHELL('',(#3276,#3277,#3278,#3279,#3280,#3281,#3282,#3283));
#3668=AXIS2_PLACEMENT_3D('',#5431,#4443,#4444);
#3669=AXIS2_PLACEMENT_3D('',#5432,#4445,#4446);
#3670=AXIS2_PLACEMENT_3D('',#5434,#4447,#4448);
#3671=AXIS2_PLACEMENT_3D('',#5435,#4449,#4450);
#3672=AXIS2_PLACEMENT_3D('',#5437,#4451,#4452);
#3673=AXIS2_PLACEMENT_3D('',#5439,#4454,#4455);
#3674=AXIS2_PLACEMENT_3D('',#5441,#4456,#4457);
#3675=AXIS2_PLACEMENT_3D('',#5443,#4459,#4460);
#3676=AXIS2_PLACEMENT_3D('',#5445,#4461,#4462);
#3677=AXIS2_PLACEMENT_3D('',#5447,#4464,#4465);
#3678=AXIS2_PLACEMENT_3D('',#5449,#4466,#4467);
#3679=AXIS2_PLACEMENT_3D('',#5450,#4468,#4469);
#3680=AXIS2_PLACEMENT_3D('',#5452,#4470,#4471);
#3681=AXIS2_PLACEMENT_3D('',#5454,#4473,#4474);
#3682=AXIS2_PLACEMENT_3D('',#5456,#4475,#4476);
#3683=AXIS2_PLACEMENT_3D('',#5458,#4478,#4479);
#3684=AXIS2_PLACEMENT_3D('',#5460,#4480,#4481);
#3685=AXIS2_PLACEMENT_3D('',#5462,#4483,#4484);
#3686=AXIS2_PLACEMENT_3D('',#5463,#4485,#4486);
#3687=AXIS2_PLACEMENT_3D('',#5472,#4491,#4492);
#3688=AXIS2_PLACEMENT_3D('',#5478,#4496,#4497);
#3689=AXIS2_PLACEMENT_3D('',#5484,#4501,#4502);
#3690=AXIS2_PLACEMENT_3D('',#5490,#4506,#4507);
#3691=AXIS2_PLACEMENT_3D('',#5496,#4511,#4512);
#3692=AXIS2_PLACEMENT_3D('',#5499,#4515,#4516);
#3693=AXIS2_PLACEMENT_3D('',#5500,#4517,#4518);
#4443=DIRECTION('axis',(0.,0.,1.));
#4444=DIRECTION('refdir',(1.,0.,0.));
#4445=DIRECTION('center_axis',(0.,1.,0.));
#4446=DIRECTION('ref_axis',(0.,0.,1.));
#4447=DIRECTION('center_axis',(0.,-1.,0.));
#4448=DIRECTION('ref_axis',(1.,0.,0.));
#4449=DIRECTION('center_axis',(0.,-1.,0.));
#4450=DIRECTION('ref_axis',(1.,0.,0.));
#4451=DIRECTION('center_axis',(0.,-1.,0.));
#4452=DIRECTION('ref_axis',(1.,0.,0.));
#4453=DIRECTION('',(0.707106781186547,0.707106781186548,8.65956056235493E-17));
#4454=DIRECTION('center_axis',(0.,-1.,0.));
#4455=DIRECTION('ref_axis',(1.,0.,0.));
#4456=DIRECTION('center_axis',(0.,-1.,0.));
#4457=DIRECTION('ref_axis',(1.,0.,0.));
#4458=DIRECTION('',(0.,1.,0.));
#4459=DIRECTION('center_axis',(0.,1.,0.));
#4460=DIRECTION('ref_axis',(1.,0.,0.));
#4461=DIRECTION('center_axis',(0.,-1.,0.));
#4462=DIRECTION('ref_axis',(1.,0.,0.));
#4463=DIRECTION('',(-0.707106781186547,0.707106781186548,-8.65956056235493E-17));
#4464=DIRECTION('center_axis',(0.,-1.,0.));
#4465=DIRECTION('ref_axis',(0.,0.,-1.));
#4466=DIRECTION('center_axis',(0.,-1.,0.));
#4467=DIRECTION('ref_axis',(1.,0.,0.));
#4468=DIRECTION('center_axis',(0.,1.,0.));
#4469=DIRECTION('ref_axis',(1.,0.,0.));
#4470=DIRECTION('center_axis',(0.,1.,0.));
#4471=DIRECTION('ref_axis',(1.,0.,0.));
#4472=DIRECTION('',(-0.447213595499958,0.894427190999916,-5.47678698264203E-17));
#4473=DIRECTION('center_axis',(0.,-1.,0.));
#4474=DIRECTION('ref_axis',(1.,0.,0.));
#4475=DIRECTION('center_axis',(0.,1.,0.));
#4476=DIRECTION('ref_axis',(1.,0.,0.));
#4477=DIRECTION('',(0.,1.,0.));
#4478=DIRECTION('center_axis',(0.,1.,0.));
#4479=DIRECTION('ref_axis',(1.,0.,0.));
#4480=DIRECTION('center_axis',(0.,-1.,0.));
#4481=DIRECTION('ref_axis',(1.,0.,0.));
#4482=DIRECTION('',(-0.707106781186547,0.707106781186548,-8.65956056235493E-17));
#4483=DIRECTION('center_axis',(0.,-1.,0.));
#4484=DIRECTION('ref_axis',(0.,0.,-1.));
#4485=DIRECTION('center_axis',(0.866025403784439,0.,-0.5));
#4486=DIRECTION('ref_axis',(0.5,0.,0.866025403784439));
#4487=DIRECTION('',(-0.5,0.,-0.866025403784439));
#4488=DIRECTION('',(0.,-1.,0.));
#4489=DIRECTION('',(0.5,0.,0.866025403784439));
#4490=DIRECTION('',(0.,-1.,0.));
#4491=DIRECTION('center_axis',(1.60246890531964E-16,0.,-1.));
#4492=DIRECTION('ref_axis',(1.,0.,1.60246890531964E-16));
#4493=DIRECTION('',(-1.,0.,-1.60246890531964E-16));
#4494=DIRECTION('',(0.,-1.,0.));
#4495=DIRECTION('',(1.,0.,1.60246890531964E-16));
#4496=DIRECTION('center_axis',(-0.866025403784439,0.,-0.5));
#4497=DIRECTION('ref_axis',(0.5,0.,-0.866025403784439));
#4498=DIRECTION('',(-0.5,0.,0.866025403784439));
#4499=DIRECTION('',(0.,-1.,0.));
#4500=DIRECTION('',(0.5,0.,-0.866025403784439));
#4501=DIRECTION('center_axis',(-0.866025403784439,0.,0.5));
#4502=DIRECTION('ref_axis',(-0.5,0.,-0.866025403784439));
#4503=DIRECTION('',(0.5,0.,0.866025403784439));
#4504=DIRECTION('',(0.,-1.,0.));
#4505=DIRECTION('',(-0.5,0.,-0.866025403784439));
#4506=DIRECTION('center_axis',(-1.60246890531964E-16,0.,1.));
#4507=DIRECTION('ref_axis',(-1.,0.,-1.60246890531964E-16));
#4508=DIRECTION('',(1.,0.,1.60246890531964E-16));
#4509=DIRECTION('',(0.,-1.,0.));
#4510=DIRECTION('',(-1.,0.,-1.60246890531964E-16));
#4511=DIRECTION('center_axis',(0.866025403784439,0.,0.5));
#4512=DIRECTION('ref_axis',(-0.5,0.,0.866025403784439));
#4513=DIRECTION('',(0.5,0.,-0.866025403784439));
#4514=DIRECTION('',(-0.5,0.,0.866025403784439));
#4515=DIRECTION('center_axis',(0.,1.,0.));
#4516=DIRECTION('ref_axis',(1.,0.,0.));
#4517=DIRECTION('center_axis',(0.,-1.,0.));
#4518=DIRECTION('ref_axis',(0.,0.,-1.));
#5431=CARTESIAN_POINT('',(0.,0.,0.));
#5432=CARTESIAN_POINT('Origin',(0.3,0.4,0.));
#5433=CARTESIAN_POINT('',(-0.3,0.4,-3.67394039744206E-17));
#5434=CARTESIAN_POINT('Origin',(0.,0.4,0.));
#5435=CARTESIAN_POINT('Origin',(0.,0.375,0.));
#5436=CARTESIAN_POINT('',(-0.35,0.35,-4.28626379701573E-17));
#5437=CARTESIAN_POINT('Origin',(0.,0.35,0.));
#5438=CARTESIAN_POINT('',(-0.325,0.375,-3.9801020972289E-17));
#5439=CARTESIAN_POINT('Origin',(0.,0.19,0.));
#5440=CARTESIAN_POINT('',(-0.35,0.03,-4.28626379701574E-17));
#5441=CARTESIAN_POINT('Origin',(0.,0.03,0.));
#5442=CARTESIAN_POINT('',(-0.35,0.19,-4.28626379701574E-17));
#5443=CARTESIAN_POINT('Origin',(0.,0.0149999999999999,0.));
#5444=CARTESIAN_POINT('',(-0.32,-3.29597460435593E-17,-3.91886975727153E-17));
#5445=CARTESIAN_POINT('Origin',(0.,0.,0.));
#5446=CARTESIAN_POINT('',(-0.335,0.0149999999999999,-4.10256677714363E-17));
#5447=CARTESIAN_POINT('Origin',(0.22,0.,0.));
#5448=CARTESIAN_POINT('',(-0.22,-6.93889390390723E-18,-2.69422295812418E-17));
#5449=CARTESIAN_POINT('Origin',(0.,0.,0.));
#5450=CARTESIAN_POINT('Origin',(0.,-0.02,0.));
#5451=CARTESIAN_POINT('',(-0.1954,-0.0492,2.39295984553393E-17));
#5452=CARTESIAN_POINT('Origin',(0.,-0.0492,0.));
#5453=CARTESIAN_POINT('',(-0.21,-0.02,-2.57175827820944E-17));
#5454=CARTESIAN_POINT('Origin',(0.,-0.8,0.));
#5455=CARTESIAN_POINT('',(-0.1954,-1.5646,2.39295984553393E-17));
#5456=CARTESIAN_POINT('Origin',(0.,-1.5646,0.));
#5457=CARTESIAN_POINT('',(-0.1954,-0.8,-2.39295984553393E-17));
#5458=CARTESIAN_POINT('Origin',(0.,-1.58,0.));
#5459=CARTESIAN_POINT('',(-0.16,-1.6,-1.95943487863577E-17));
#5460=CARTESIAN_POINT('Origin',(0.,-1.6,0.));
#5461=CARTESIAN_POINT('',(-0.18,-1.58,-2.20436423846524E-17));
#5462=CARTESIAN_POINT('Origin',(0.,-1.6,0.));
#5463=CARTESIAN_POINT('Origin',(0.0866025403784439,-0.4,-0.15));
#5464=CARTESIAN_POINT('',(0.173205080756888,-0.4,0.));
#5465=CARTESIAN_POINT('',(0.0866025403784439,-0.4,-0.15));
#5466=CARTESIAN_POINT('',(0.173205080756888,-0.4,0.));
#5467=CARTESIAN_POINT('',(0.0866025403784439,-0.64,-0.15));
#5468=CARTESIAN_POINT('',(0.0866025403784439,-0.4,-0.15));
#5469=CARTESIAN_POINT('',(0.173205080756888,-0.64,0.));
#5470=CARTESIAN_POINT('',(0.173205080756888,-0.64,0.));
#5471=CARTESIAN_POINT('',(0.173205080756888,-0.4,0.));
#5472=CARTESIAN_POINT('Origin',(-0.0866025403784438,-0.4,-0.15));
#5473=CARTESIAN_POINT('',(-0.0866025403784438,-0.4,-0.15));
#5474=CARTESIAN_POINT('',(0.0866025403784439,-0.4,-0.15));
#5475=CARTESIAN_POINT('',(-0.0866025403784438,-0.64,-0.15));
#5476=CARTESIAN_POINT('',(-0.0866025403784438,-0.4,-0.15));
#5477=CARTESIAN_POINT('',(0.0866025403784439,-0.64,-0.15));
#5478=CARTESIAN_POINT('Origin',(-0.173205080756888,-0.4,-2.77555756156289E-17));
#5479=CARTESIAN_POINT('',(-0.173205080756888,-0.4,-2.12115047744981E-17));
#5480=CARTESIAN_POINT('',(-0.0866025403784438,-0.4,-0.15));
#5481=CARTESIAN_POINT('',(-0.173205080756888,-0.64,-2.77555756156289E-17));
#5482=CARTESIAN_POINT('',(-0.173205080756888,-0.4,-2.12115047744981E-17));
#5483=CARTESIAN_POINT('',(-0.0866025403784438,-0.64,-0.15));
#5484=CARTESIAN_POINT('Origin',(-0.0866025403784439,-0.4,0.15));
#5485=CARTESIAN_POINT('',(-0.0866025403784439,-0.4,0.15));
#5486=CARTESIAN_POINT('',(-0.173205080756888,-0.4,-2.12115047744981E-17));
#5487=CARTESIAN_POINT('',(-0.0866025403784439,-0.64,0.15));
#5488=CARTESIAN_POINT('',(-0.0866025403784439,-0.4,0.15));
#5489=CARTESIAN_POINT('',(-0.173205080756888,-0.64,-2.12115047744981E-17));
#5490=CARTESIAN_POINT('Origin',(0.0866025403784439,-0.4,0.15));
#5491=CARTESIAN_POINT('',(0.0866025403784439,-0.4,0.15));
#5492=CARTESIAN_POINT('',(-0.0866025403784439,-0.4,0.15));
#5493=CARTESIAN_POINT('',(0.0866025403784439,-0.64,0.15));
#5494=CARTESIAN_POINT('',(0.0866025403784439,-0.4,0.15));
#5495=CARTESIAN_POINT('',(-0.0866025403784439,-0.64,0.15));
#5496=CARTESIAN_POINT('Origin',(0.173205080756888,-0.4,0.));
#5497=CARTESIAN_POINT('',(0.0866025403784439,-0.4,0.15));
#5498=CARTESIAN_POINT('',(0.0866025403784439,-0.64,0.15));
#5499=CARTESIAN_POINT('Origin',(0.,-0.4,-2.77555756156289E-17));
#5500=CARTESIAN_POINT('Origin',(0.,-0.64,-2.77555756156289E-17));
#5741=UNCERTAINTY_MEASURE_WITH_UNIT(LENGTH_MEASURE(0.001),#5762,
'DISTANCE_ACCURACY_VALUE',
'Maximum model space distance between geometric entities at asserted c
onnectivities');
#5745=UNCERTAINTY_MEASURE_WITH_UNIT(LENGTH_MEASURE(0.001),#5762,
'DISTANCE_ACCURACY_VALUE',
'Maximum model space distance between geometric entities at asserted c
onnectivities');
#5757=(
GEOMETRIC_REPRESENTATION_CONTEXT(3)
GLOBAL_UNCERTAINTY_ASSIGNED_CONTEXT((#5741))
GLOBAL_UNIT_ASSIGNED_CONTEXT((#5762,#5764,#5765))
REPRESENTATION_CONTEXT('','3D')
);
#5761=(
GEOMETRIC_REPRESENTATION_CONTEXT(3)
GLOBAL_UNCERTAINTY_ASSIGNED_CONTEXT((#5745))
GLOBAL_UNIT_ASSIGNED_CONTEXT((#5762,#5764,#5765))
REPRESENTATION_CONTEXT('','3D')
);
#5762=(
LENGTH_UNIT()
NAMED_UNIT(*)
SI_UNIT(.CENTI.,.METRE.)
);
#5764=(
NAMED_UNIT(*)
PLANE_ANGLE_UNIT()
SI_UNIT($,.RADIAN.)
);
#5765=(
NAMED_UNIT(*)
SI_UNIT($,.STERADIAN.)
SOLID_ANGLE_UNIT()
);
#5777=SHAPE_DEFINITION_REPRESENTATION(#5792,#5826);
#5792=PRODUCT_DEFINITION_SHAPE('',$,#5842);
#5826=SHAPE_REPRESENTATION('',(#3668),#5757);
#5830=PRODUCT_DEFINITION_CONTEXT('part definition',#5877,'design');
#5842=PRODUCT_DEFINITION('Cap Screw - M4x16','Cap Screw - M4x16',#5857,
#5830);
#5857=PRODUCT_DEFINITION_FORMATION('',$,#5890);
#5877=APPLICATION_CONTEXT(
'Core Data for Automotive Mechanical Design Process');
#5878=PRODUCT_CONTEXT('part definition',#5877,'mechanical');
#5890=PRODUCT('Cap Screw - M4x16','Cap Screw - M4x16',
'Cap Screw - M4x16',(#5878));
#5950=COLOUR_RGB('Black',0.12,0.14,0.17);
#5951=FILL_AREA_STYLE_COLOUR('',#5950);
#5952=FILL_AREA_STYLE('',(#5951));
#5953=SURFACE_STYLE_FILL_AREA(#5952);
#5954=SURFACE_SIDE_STYLE('',(#5953));
#5955=SURFACE_STYLE_USAGE(.BOTH.,#5954);
#5956=PRESENTATION_STYLE_ASSIGNMENT((#5955));
ENDSEC;
END-ISO-10303-21;
